ISO-10303-21;
HEADER;
/* Generated by software containing ST-Developer
 * from STEP Tools, Inc. (www.steptools.com) 
 */

FILE_DESCRIPTION(
/* description */ ('Gravity roller conveyor section'),
/* implementation_level */ '2;1');

FILE_NAME(
/* name */ 'Flat Washer - M5.step',
/* time_stamp */ '2026-11-02T07:43:02-08:00',
/* author */ (''),
/* organization */ (''),
/* preprocessor_version */ 'ST-DEVELOPER v20.2',
/* originating_system */ 'Autodesk Translation Framework v15.17.0.0',
/* authorisation */ '');

FILE_SCHEMA (('AUTOMOTIVE_DESIGN { 1 0 10303 214 3 1 1 }'));
ENDSEC;

DATA;
#10=MECHANICAL_DESIGN_GEOMETRIC_PRESENTATION_REPRESENTATION('',(#536),#13821);
#414=CONICAL_SURFACE('',#8301,0.275,0.785398163397449);
#468=SHAPE_REPRESENTATION_RELATIONSHIP('SRR','None',#14005,#502);
#502=ADVANCED_BREP_SHAPE_REPRESENTATION('',(#576),#13792);
#536=STYLED_ITEM('',(#14191),#576);
#576=MANIFOLD_SOLID_BREP('Body1',#7636);
#640=FACE_BOUND('',#1660,.T.);
#641=FACE_BOUND('',#1663,.T.);
#875=PLANE('',#8306);
#876=PLANE('',#8310);
#1207=FACE_OUTER_BOUND('',#1657,.T.);
#1208=FACE_OUTER_BOUND('',#1658,.T.);
#1209=FACE_OUTER_BOUND('',#1659,.T.);
#1210=FACE_OUTER_BOUND('',#1661,.T.);
#1211=FACE_OUTER_BOUND('',#1662,.T.);
#1657=EDGE_LOOP('',(#6278,#6279,#6280,#6281));
#1658=EDGE_LOOP('',(#6282,#6283,#6284,#6285));
#1659=EDGE_LOOP('',(#6286));
#1660=EDGE_LOOP('',(#6287));
#1661=EDGE_LOOP('',(#6288,#6289,#6290,#6291));
#1662=EDGE_LOOP('',(#6292));
#1663=EDGE_LOOP('',(#6293));
#2423=LINE('',#12352,#3141);
#2424=LINE('',#12356,#3142);
#2425=LINE('',#12363,#3143);
#3141=VECTOR('',#9812,0.275);
#3142=VECTOR('',#9817,0.265);
#3143=VECTOR('',#9826,0.5);
#3417=CIRCLE('',#8302,0.285);
#3418=CIRCLE('',#8303,0.265);
#3419=CIRCLE('',#8305,0.265);
#3420=CIRCLE('',#8307,0.5);
#3421=CIRCLE('',#8309,0.5);
#3947=VERTEX_POINT('',#12349);
#3948=VERTEX_POINT('',#12351);
#3949=VERTEX_POINT('',#12355);
#3950=VERTEX_POINT('',#12359);
#3951=VERTEX_POINT('',#12362);
#4776=EDGE_CURVE('',#3947,#3947,#3417,.T.);
#4777=EDGE_CURVE('',#3947,#3948,#2423,.T.);
#4778=EDGE_CURVE('',#3948,#3948,#3418,.T.);
#4779=EDGE_CURVE('',#3948,#3949,#2424,.T.);
#4780=EDGE_CURVE('',#3949,#3949,#3419,.T.);
#4781=EDGE_CURVE('',#3950,#3950,#3420,.T.);
#4782=EDGE_CURVE('',#3950,#3951,#2425,.T.);
#4783=EDGE_CURVE('',#3951,#3951,#3421,.T.);
#6278=ORIENTED_EDGE('',*,*,#4776,.T.);
#6279=ORIENTED_EDGE('',*,*,#4777,.T.);
#6280=ORIENTED_EDGE('',*,*,#4778,.T.);
#6281=ORIENTED_EDGE('',*,*,#4777,.F.);
#6282=ORIENTED_EDGE('',*,*,#4778,.F.);
#6283=ORIENTED_EDGE('',*,*,#4779,.T.);
#6284=ORIENTED_EDGE('',*,*,#4780,.T.);
#6285=ORIENTED_EDGE('',*,*,#4779,.F.);
#6286=ORIENTED_EDGE('',*,*,#4781,.T.);
#6287=ORIENTED_EDGE('',*,*,#4776,.F.);
#6288=ORIENTED_EDGE('',*,*,#4781,.F.);
#6289=ORIENTED_EDGE('',*,*,#4782,.T.);
#6290=ORIENTED_EDGE('',*,*,#4783,.T.);
#6291=ORIENTED_EDGE('',*,*,#4782,.F.);
#6292=ORIENTED_EDGE('',*,*,#4783,.F.);
#6293=ORIENTED_EDGE('',*,*,#4780,.F.);
#7150=CYLINDRICAL_SURFACE('',#8304,0.265);
#7151=CYLINDRICAL_SURFACE('',#8308,0.5);
#7408=ADVANCED_FACE('',(#1207),#414,.F.);
#7409=ADVANCED_FACE('',(#1208),#7150,.F.);
#7410=ADVANCED_FACE('',(#1209,#640),#875,.T.);
#7411=ADVANCED_FACE('',(#1210),#7151,.T.);
#7412=ADVANCED_FACE('',(#1211,#641),#876,.F.);
#7636=CLOSED_SHELL('',(#7408,#7409,#7410,#7411,#7412));
#8300=AXIS2_PLACEMENT_3D('',#12347,#9806,#9807);
#8301=AXIS2_PLACEMENT_3D('',#12348,#9808,#9809);
#8302=AXIS2_PLACEMENT_3D('',#12350,#9810,#9811);
#8303=AXIS2_PLACEMENT_3D('',#12353,#9813,#9814);
#8304=AXIS2_PLACEMENT_3D('',#12354,#9815,#9816);
#8305=AXIS2_PLACEMENT_3D('',#12357,#9818,#9819);
#8306=AXIS2_PLACEMENT_3D('',#12358,#9820,#9821);
#8307=AXIS2_PLACEMENT_3D('',#12360,#9822,#9823);
#8308=AXIS2_PLACEMENT_3D('',#12361,#9824,#9825);
#8309=AXIS2_PLACEMENT_3D('',#12364,#9827,#9828);
#8310=AXIS2_PLACEMENT_3D('',#12365,#9829,#9830);
#9806=DIRECTION('axis',(0.,0.,1.));
#9807=DIRECTION('refdir',(1.,0.,0.));
#9808=DIRECTION('center_axis',(0.,1.,0.));
#9809=DIRECTION('ref_axis',(1.,0.,0.));
#9810=DIRECTION('center_axis',(0.,1.,0.));
#9811=DIRECTION('ref_axis',(1.,0.,0.));
#9812=DIRECTION('',(0.707106781186548,-0.707106781186547,-8.65956056235494E-17));
#9813=DIRECTION('center_axis',(0.,-1.,0.));
#9814=DIRECTION('ref_axis',(1.,0.,0.));
#9815=DIRECTION('center_axis',(0.,1.,0.));
#9816=DIRECTION('ref_axis',(1.,0.,0.));
#9817=DIRECTION('',(0.,-1.,0.));
#9818=DIRECTION('center_axis',(0.,-1.,0.));
#9819=DIRECTION('ref_axis',(1.,0.,0.));
#9820=DIRECTION('center_axis',(0.,1.,0.));
#9821=DIRECTION('ref_axis',(1.,0.,0.));
#9822=DIRECTION('center_axis',(0.,1.,0.));
#9823=DIRECTION('ref_axis',(1.,0.,0.));
#9824=DIRECTION('center_axis',(0.,1.,0.));
#9825=DIRECTION('ref_axis',(1.,0.,0.));
#9826=DIRECTION('',(0.,-1.,0.));
#9827=DIRECTION('center_axis',(0.,1.,0.));
#9828=DIRECTION('ref_axis',(1.,0.,0.));
#9829=DIRECTION('center_axis',(0.,1.,0.));
#9830=DIRECTION('ref_axis',(1.,0.,0.));
#12347=CARTESIAN_POINT('',(0.,0.,0.));
#12348=CARTESIAN_POINT('Origin',(0.,0.09,0.));
#12349=CARTESIAN_POINT('',(-0.285,0.1,3.49024337756996E-17));
#12350=CARTESIAN_POINT('Origin',(0.,0.1,0.));
#12351=CARTESIAN_POINT('',(-0.265,0.08,-3.24531401774049E-17));
#12352=CARTESIAN_POINT('',(-0.275,0.09,3.36777869765522E-17));
#12353=CARTESIAN_POINT('Origin',(0.,0.08,0.));
#12354=CARTESIAN_POINT('Origin',(0.,0.,0.));
#12355=CARTESIAN_POINT('',(-0.265,0.,3.24531401774049E-17));
#12356=CARTESIAN_POINT('',(-0.265,0.,3.24531401774049E-17));
#12357=CARTESIAN_POINT('Origin',(0.,0.,0.));
#12358=CARTESIAN_POINT('Origin',(0.,0.1,0.));
#12359=CARTESIAN_POINT('',(-0.5,0.1,6.12323399573677E-17));
#12360=CARTESIAN_POINT('Origin',(0.,0.1,0.));
#12361=CARTESIAN_POINT('Origin',(0.,0.,0.));
#12362=CARTESIAN_POINT('',(-0.5,0.,6.12323399573677E-17));
#12363=CARTESIAN_POINT('',(-0.5,0.,6.12323399573677E-17));
#12364=CARTESIAN_POINT('Origin',(0.,0.,0.));
#12365=CARTESIAN_POINT('Origin',(0.,0.,0.));
#13753=UNCERTAINTY_MEASURE_WITH_UNIT(LENGTH_MEASURE(0.001),#13822,
'DISTANCE_ACCURACY_VALUE',
'Maximum model space distance between geometric entities at asserted c
onnectivities');
#13782=UNCERTAINTY_MEASURE_WITH_UNIT(LENGTH_MEASURE(0.001),#13822,
'DISTANCE_ACCURACY_VALUE',
'Maximum model space distance between geometric entities at asserted c
onnectivities');
#13792=(
GEOMETRIC_REPRESENTATION_CONTEXT(3)
GLOBAL_UNCERTAINTY_ASSIGNED_CONTEXT((#13753))
GLOBAL_UNIT_ASSIGNED_CONTEXT((#13822,#13824,#13825))
REPRESENTATION_CONTEXT('','3D')
);
#13821=(
GEOMETRIC_REPRESENTATION_CONTEXT(3)
GLOBAL_UNCERTAINTY_ASSIGNED_CONTEXT((#13782))
GLOBAL_UNIT_ASSIGNED_CONTEXT((#13822,#13824,#13825))
REPRESENTATION_CONTEXT('','3D')
);
#13822=(
LENGTH_UNIT()
NAMED_UNIT(*)
SI_UNIT(.CENTI.,.METRE.)
);
#13824=(
NAMED_UNIT(*)
PLANE_ANGLE_UNIT()
SI_UNIT($,.RADIAN.)
);
#13825=(
NAMED_UNIT(*)
SI_UNIT($,.STERADIAN.)
SOLID_ANGLE_UNIT()
);
#13835=SHAPE_DEFINITION_REPRESENTATION(#13873,#14005);
#13873=PRODUCT_DEFINITION_SHAPE('',$,#14044);
#14005=SHAPE_REPRESENTATION('',(#8300),#13792);
#14034=PRODUCT_DEFINITION_CONTEXT('part definition',#14150,'design');
#14044=PRODUCT_DEFINITION('Flat Washer - M5','Flat Washer - M5',#14082,
#14034);
#14082=PRODUCT_DEFINITION_FORMATION('',$,#14161);
#14150=APPLICATION_CONTEXT(
'Core Data for Automotive Mechanical Design Process');
#14151=PRODUCT_CONTEXT('part definition',#14150,'mechanical');
#14161=PRODUCT('Flat Washer - M5','Flat Washer - M5','Flat Washer - M5',
(#14151));
#14191=PRESENTATION_STYLE_ASSIGNMENT((#14196));
#14196=SURFACE_STYLE_USAGE(.BOTH.,#14201);
#14201=SURFACE_SIDE_STYLE('',(#14206));
#14206=SURFACE_STYLE_FILL_AREA(#14211);
#14211=FILL_AREA_STYLE('CAD Library Painted - Steel gray',(#14216));
#14216=FILL_AREA_STYLE_COLOUR('CAD Library Painted - Steel gray',#14221);
#14221=COLOUR_RGB('CAD Library Painted - Steel gray',0.592156862745098,
0.631372549019608,0.67843137254902);
ENDSEC;
END-ISO-10303-21;
